ISO-10303-21;
HEADER;
/* Generated by software containing ST-Developer
 * from STEP Tools, Inc. (www.steptools.com) 
 */

FILE_DESCRIPTION(
/* description */ ('PAT-003'),
/* implementation_level */ '2;1');

FILE_NAME(
/* name */ 'Captive slot nut.step',
/* time_stamp */ '2026-10-29T15:45:40-07:00',
/* author */ (''),
/* organization */ (''),
/* preprocessor_version */ 'ST-DEVELOPER v20.2',
/* originating_system */ 'Autodesk Translation Framework v15.17.0.0',
/* authorisation */ '');

FILE_SCHEMA (('AUTOMOTIVE_DESIGN { 1 0 10303 214 3 1 1 }'));
ENDSEC;

DATA;
#10=MECHANICAL_DESIGN_GEOMETRIC_PRESENTATION_REPRESENTATION('',(#148),#5761);
#121=ELLIPSE('',#3509,0.299389011154384,0.2117);
#122=ELLIPSE('',#3513,0.299389011154384,0.2117);
#124=SHAPE_REPRESENTATION_RELATIONSHIP('SRR','None',#5818,#136);
#136=ADVANCED_BREP_SHAPE_REPRESENTATION('',(#160),#5749);
#148=STYLED_ITEM('',(#5956),#160);
#160=MANIFOLD_SOLID_BREP('Body1',#3322);
#178=FACE_BOUND('',#555,.T.);
#215=PLANE('',#3499);
#216=PLANE('',#3500);
#217=PLANE('',#3501);
#218=PLANE('',#3503);
#219=PLANE('',#3504);
#220=PLANE('',#3505);
#221=PLANE('',#3506);
#222=PLANE('',#3507);
#223=PLANE('',#3508);
#224=PLANE('',#3515);
#225=PLANE('',#3516);
#226=PLANE('',#3517);
#227=PLANE('',#3518);
#356=FACE_OUTER_BOUND('',#552,.T.);
#357=FACE_OUTER_BOUND('',#553,.T.);
#358=FACE_OUTER_BOUND('',#554,.T.);
#359=FACE_OUTER_BOUND('',#556,.T.);
#360=FACE_OUTER_BOUND('',#557,.T.);
#361=FACE_OUTER_BOUND('',#558,.T.);
#362=FACE_OUTER_BOUND('',#559,.T.);
#363=FACE_OUTER_BOUND('',#560,.T.);
#364=FACE_OUTER_BOUND('',#561,.T.);
#365=FACE_OUTER_BOUND('',#562,.T.);
#366=FACE_OUTER_BOUND('',#563,.T.);
#367=FACE_OUTER_BOUND('',#564,.T.);
#368=FACE_OUTER_BOUND('',#565,.T.);
#369=FACE_OUTER_BOUND('',#566,.T.);
#552=EDGE_LOOP('',(#2278,#2279,#2280,#2281));
#553=EDGE_LOOP('',(#2282,#2283,#2284,#2285));
#554=EDGE_LOOP('',(#2286,#2287,#2288,#2289));
#555=EDGE_LOOP('',(#2290));
#556=EDGE_LOOP('',(#2291,#2292,#2293,#2294,#2295,#2296,#2297,#2298,#2299,
#2300));
#557=EDGE_LOOP('',(#2301,#2302,#2303,#2304));
#558=EDGE_LOOP('',(#2305,#2306,#2307,#2308));
#559=EDGE_LOOP('',(#2309,#2310,#2311,#2312,#2313,#2314,#2315,#2316,#2317,
#2318));
#560=EDGE_LOOP('',(#2319,#2320,#2321,#2322));
#561=EDGE_LOOP('',(#2323,#2324,#2325,#2326,#2327,#2328));
#562=EDGE_LOOP('',(#2329,#2330,#2331,#2332,#2333,#2334,#2335,#2336));
#563=EDGE_LOOP('',(#2337,#2338,#2339,#2340,#2341));
#564=EDGE_LOOP('',(#2342,#2343,#2344,#2345));
#565=EDGE_LOOP('',(#2346,#2347,#2348,#2349,#2350,#2351));
#566=EDGE_LOOP('',(#2352,#2353,#2354,#2355));
#770=LINE('',#4819,#1092);
#771=LINE('',#4821,#1093);
#772=LINE('',#4823,#1094);
#773=LINE('',#4824,#1095);
#774=LINE('',#4827,#1096);
#775=LINE('',#4829,#1097);
#776=LINE('',#4830,#1098);
#777=LINE('',#4833,#1099);
#778=LINE('',#4835,#1100);
#779=LINE('',#4836,#1101);
#780=LINE('',#4841,#1102);
#781=LINE('',#4843,#1103);
#782=LINE('',#4845,#1104);
#783=LINE('',#4847,#1105);
#784=LINE('',#4849,#1106);
#785=LINE('',#4851,#1107);
#786=LINE('',#4852,#1108);
#787=LINE('',#4855,#1109);
#788=LINE('',#4856,#1110);
#789=LINE('',#4859,#1111);
#790=LINE('',#4860,#1112);
#791=LINE('',#4863,#1113);
#792=LINE('',#4865,#1114);
#793=LINE('',#4867,#1115);
#794=LINE('',#4869,#1116);
#795=LINE('',#4870,#1117);
#796=LINE('',#4872,#1118);
#797=LINE('',#4875,#1119);
#798=LINE('',#4878,#1120);
#799=LINE('',#4882,#1121);
#800=LINE('',#4889,#1122);
#801=LINE('',#4891,#1123);
#802=LINE('',#4893,#1124);
#1092=VECTOR('',#3869,1.);
#1093=VECTOR('',#3870,1.);
#1094=VECTOR('',#3871,1.);
#1095=VECTOR('',#3872,1.);
#1096=VECTOR('',#3875,1.);
#1097=VECTOR('',#3876,1.);
#1098=VECTOR('',#3877,1.);
#1099=VECTOR('',#3880,1.);
#1100=VECTOR('',#3881,1.);
#1101=VECTOR('',#3882,1.);
#1102=VECTOR('',#3887,1.);
#1103=VECTOR('',#3888,1.);
#1104=VECTOR('',#3889,1.);
#1105=VECTOR('',#3890,1.);
#1106=VECTOR('',#3891,1.);
#1107=VECTOR('',#3892,1.);
#1108=VECTOR('',#3893,1.);
#1109=VECTOR('',#3896,1.);
#1110=VECTOR('',#3897,1.);
#1111=VECTOR('',#3900,1.);
#1112=VECTOR('',#3901,1.);
#1113=VECTOR('',#3904,1.);
#1114=VECTOR('',#3905,1.);
#1115=VECTOR('',#3906,1.);
#1116=VECTOR('',#3907,1.);
#1117=VECTOR('',#3908,1.);
#1118=VECTOR('',#3911,1.);
#1119=VECTOR('',#3914,1.);
#1120=VECTOR('',#3917,1.);
#1121=VECTOR('',#3922,0.21);
#1122=VECTOR('',#3931,1.);
#1123=VECTOR('',#3934,1.);
#1124=VECTOR('',#3937,1.);
#1408=CIRCLE('',#3502,0.2117);
#1409=CIRCLE('',#3511,0.2117);
#1410=CIRCLE('',#3512,0.2117);
#1411=CIRCLE('',#3514,0.2117);
#1512=VERTEX_POINT('',#4817);
#1513=VERTEX_POINT('',#4818);
#1514=VERTEX_POINT('',#4820);
#1515=VERTEX_POINT('',#4822);
#1516=VERTEX_POINT('',#4826);
#1517=VERTEX_POINT('',#4828);
#1518=VERTEX_POINT('',#4832);
#1519=VERTEX_POINT('',#4834);
#1520=VERTEX_POINT('',#4837);
#1521=VERTEX_POINT('',#4840);
#1522=VERTEX_POINT('',#4842);
#1523=VERTEX_POINT('',#4844);
#1524=VERTEX_POINT('',#4846);
#1525=VERTEX_POINT('',#4848);
#1526=VERTEX_POINT('',#4850);
#1527=VERTEX_POINT('',#4854);
#1528=VERTEX_POINT('',#4858);
#1529=VERTEX_POINT('',#4862);
#1530=VERTEX_POINT('',#4864);
#1531=VERTEX_POINT('',#4866);
#1532=VERTEX_POINT('',#4868);
#1533=VERTEX_POINT('',#4874);
#1534=VERTEX_POINT('',#4876);
#1535=VERTEX_POINT('',#4880);
#1536=VERTEX_POINT('',#4883);
#1537=VERTEX_POINT('',#4885);
#1810=EDGE_CURVE('',#1512,#1513,#770,.T.);
#1811=EDGE_CURVE('',#1514,#1512,#771,.T.);
#1812=EDGE_CURVE('',#1515,#1514,#772,.T.);
#1813=EDGE_CURVE('',#1513,#1515,#773,.T.);
#1814=EDGE_CURVE('',#1514,#1516,#774,.T.);
#1815=EDGE_CURVE('',#1517,#1516,#775,.T.);
#1816=EDGE_CURVE('',#1515,#1517,#776,.T.);
#1817=EDGE_CURVE('',#1516,#1518,#777,.T.);
#1818=EDGE_CURVE('',#1518,#1519,#778,.T.);
#1819=EDGE_CURVE('',#1519,#1517,#779,.T.);
#1820=EDGE_CURVE('',#1520,#1520,#1408,.T.);
#1821=EDGE_CURVE('',#1521,#1512,#780,.T.);
#1822=EDGE_CURVE('',#1522,#1521,#781,.T.);
#1823=EDGE_CURVE('',#1522,#1523,#782,.T.);
#1824=EDGE_CURVE('',#1524,#1523,#783,.T.);
#1825=EDGE_CURVE('',#1524,#1525,#784,.T.);
#1826=EDGE_CURVE('',#1525,#1526,#785,.T.);
#1827=EDGE_CURVE('',#1526,#1518,#786,.T.);
#1828=EDGE_CURVE('',#1526,#1527,#787,.T.);
#1829=EDGE_CURVE('',#1527,#1519,#788,.T.);
#1830=EDGE_CURVE('',#1528,#1525,#789,.T.);
#1831=EDGE_CURVE('',#1527,#1528,#790,.T.);
#1832=EDGE_CURVE('',#1529,#1528,#791,.T.);
#1833=EDGE_CURVE('',#1530,#1529,#792,.T.);
#1834=EDGE_CURVE('',#1530,#1531,#793,.T.);
#1835=EDGE_CURVE('',#1532,#1531,#794,.T.);
#1836=EDGE_CURVE('',#1532,#1513,#795,.T.);
#1837=EDGE_CURVE('',#1529,#1524,#796,.T.);
#1838=EDGE_CURVE('',#1523,#1533,#797,.T.);
#1839=EDGE_CURVE('',#1533,#1534,#121,.T.);
#1840=EDGE_CURVE('',#1534,#1530,#798,.T.);
#1841=EDGE_CURVE('',#1535,#1533,#1409,.F.);
#1842=EDGE_CURVE('',#1535,#1520,#799,.T.);
#1843=EDGE_CURVE('',#1536,#1535,#1410,.F.);
#1844=EDGE_CURVE('',#1537,#1536,#122,.T.);
#1845=EDGE_CURVE('',#1534,#1537,#1411,.F.);
#1846=EDGE_CURVE('',#1536,#1522,#800,.T.);
#1847=EDGE_CURVE('',#1531,#1537,#801,.T.);
#1848=EDGE_CURVE('',#1521,#1532,#802,.T.);
#2278=ORIENTED_EDGE('',*,*,#1810,.F.);
#2279=ORIENTED_EDGE('',*,*,#1811,.F.);
#2280=ORIENTED_EDGE('',*,*,#1812,.F.);
#2281=ORIENTED_EDGE('',*,*,#1813,.F.);
#2282=ORIENTED_EDGE('',*,*,#1812,.T.);
#2283=ORIENTED_EDGE('',*,*,#1814,.T.);
#2284=ORIENTED_EDGE('',*,*,#1815,.F.);
#2285=ORIENTED_EDGE('',*,*,#1816,.F.);
#2286=ORIENTED_EDGE('',*,*,#1817,.T.);
#2287=ORIENTED_EDGE('',*,*,#1818,.T.);
#2288=ORIENTED_EDGE('',*,*,#1819,.T.);
#2289=ORIENTED_EDGE('',*,*,#1815,.T.);
#2290=ORIENTED_EDGE('',*,*,#1820,.T.);
#2291=ORIENTED_EDGE('',*,*,#1817,.F.);
#2292=ORIENTED_EDGE('',*,*,#1814,.F.);
#2293=ORIENTED_EDGE('',*,*,#1811,.T.);
#2294=ORIENTED_EDGE('',*,*,#1821,.F.);
#2295=ORIENTED_EDGE('',*,*,#1822,.F.);
#2296=ORIENTED_EDGE('',*,*,#1823,.T.);
#2297=ORIENTED_EDGE('',*,*,#1824,.F.);
#2298=ORIENTED_EDGE('',*,*,#1825,.T.);
#2299=ORIENTED_EDGE('',*,*,#1826,.T.);
#2300=ORIENTED_EDGE('',*,*,#1827,.T.);
#2301=ORIENTED_EDGE('',*,*,#1828,.T.);
#2302=ORIENTED_EDGE('',*,*,#1829,.T.);
#2303=ORIENTED_EDGE('',*,*,#1818,.F.);
#2304=ORIENTED_EDGE('',*,*,#1827,.F.);
#2305=ORIENTED_EDGE('',*,*,#1830,.F.);
#2306=ORIENTED_EDGE('',*,*,#1831,.F.);
#2307=ORIENTED_EDGE('',*,*,#1828,.F.);
#2308=ORIENTED_EDGE('',*,*,#1826,.F.);
#2309=ORIENTED_EDGE('',*,*,#1819,.F.);
#2310=ORIENTED_EDGE('',*,*,#1829,.F.);
#2311=ORIENTED_EDGE('',*,*,#1831,.T.);
#2312=ORIENTED_EDGE('',*,*,#1832,.F.);
#2313=ORIENTED_EDGE('',*,*,#1833,.F.);
#2314=ORIENTED_EDGE('',*,*,#1834,.T.);
#2315=ORIENTED_EDGE('',*,*,#1835,.F.);
#2316=ORIENTED_EDGE('',*,*,#1836,.T.);
#2317=ORIENTED_EDGE('',*,*,#1813,.T.);
#2318=ORIENTED_EDGE('',*,*,#1816,.T.);
#2319=ORIENTED_EDGE('',*,*,#1830,.T.);
#2320=ORIENTED_EDGE('',*,*,#1825,.F.);
#2321=ORIENTED_EDGE('',*,*,#1837,.F.);
#2322=ORIENTED_EDGE('',*,*,#1832,.T.);
#2323=ORIENTED_EDGE('',*,*,#1833,.T.);
#2324=ORIENTED_EDGE('',*,*,#1837,.T.);
#2325=ORIENTED_EDGE('',*,*,#1824,.T.);
#2326=ORIENTED_EDGE('',*,*,#1838,.T.);
#2327=ORIENTED_EDGE('',*,*,#1839,.T.);
#2328=ORIENTED_EDGE('',*,*,#1840,.T.);
#2329=ORIENTED_EDGE('',*,*,#1839,.F.);
#2330=ORIENTED_EDGE('',*,*,#1841,.F.);
#2331=ORIENTED_EDGE('',*,*,#1842,.T.);
#2332=ORIENTED_EDGE('',*,*,#1820,.F.);
#2333=ORIENTED_EDGE('',*,*,#1842,.F.);
#2334=ORIENTED_EDGE('',*,*,#1843,.F.);
#2335=ORIENTED_EDGE('',*,*,#1844,.F.);
#2336=ORIENTED_EDGE('',*,*,#1845,.F.);
#2337=ORIENTED_EDGE('',*,*,#1838,.F.);
#2338=ORIENTED_EDGE('',*,*,#1823,.F.);
#2339=ORIENTED_EDGE('',*,*,#1846,.F.);
#2340=ORIENTED_EDGE('',*,*,#1843,.T.);
#2341=ORIENTED_EDGE('',*,*,#1841,.T.);
#2342=ORIENTED_EDGE('',*,*,#1840,.F.);
#2343=ORIENTED_EDGE('',*,*,#1845,.T.);
#2344=ORIENTED_EDGE('',*,*,#1847,.F.);
#2345=ORIENTED_EDGE('',*,*,#1834,.F.);
#2346=ORIENTED_EDGE('',*,*,#1822,.T.);
#2347=ORIENTED_EDGE('',*,*,#1848,.T.);
#2348=ORIENTED_EDGE('',*,*,#1835,.T.);
#2349=ORIENTED_EDGE('',*,*,#1847,.T.);
#2350=ORIENTED_EDGE('',*,*,#1844,.T.);
#2351=ORIENTED_EDGE('',*,*,#1846,.T.);
#2352=ORIENTED_EDGE('',*,*,#1810,.T.);
#2353=ORIENTED_EDGE('',*,*,#1836,.F.);
#2354=ORIENTED_EDGE('',*,*,#1848,.F.);
#2355=ORIENTED_EDGE('',*,*,#1821,.T.);
#3100=CYLINDRICAL_SURFACE('',#3510,0.2117);
#3149=ADVANCED_FACE('',(#356),#215,.F.);
#3150=ADVANCED_FACE('',(#357),#216,.T.);
#3151=ADVANCED_FACE('',(#358,#178),#217,.T.);
#3152=ADVANCED_FACE('',(#359),#218,.T.);
#3153=ADVANCED_FACE('',(#360),#219,.T.);
#3154=ADVANCED_FACE('',(#361),#220,.F.);
#3155=ADVANCED_FACE('',(#362),#221,.T.);
#3156=ADVANCED_FACE('',(#363),#222,.T.);
#3157=ADVANCED_FACE('',(#364),#223,.T.);
#3158=ADVANCED_FACE('',(#365),#3100,.F.);
#3159=ADVANCED_FACE('',(#366),#224,.F.);
#3160=ADVANCED_FACE('',(#367),#225,.F.);
#3161=ADVANCED_FACE('',(#368),#226,.T.);
#3162=ADVANCED_FACE('',(#369),#227,.T.);
#3322=CLOSED_SHELL('',(#3149,#3150,#3151,#3152,#3153,#3154,#3155,#3156,
#3157,#3158,#3159,#3160,#3161,#3162));
#3498=AXIS2_PLACEMENT_3D('',#4815,#3865,#3866);
#3499=AXIS2_PLACEMENT_3D('',#4816,#3867,#3868);
#3500=AXIS2_PLACEMENT_3D('',#4825,#3873,#3874);
#3501=AXIS2_PLACEMENT_3D('',#4831,#3878,#3879);
#3502=AXIS2_PLACEMENT_3D('',#4838,#3883,#3884);
#3503=AXIS2_PLACEMENT_3D('',#4839,#3885,#3886);
#3504=AXIS2_PLACEMENT_3D('',#4853,#3894,#3895);
#3505=AXIS2_PLACEMENT_3D('',#4857,#3898,#3899);
#3506=AXIS2_PLACEMENT_3D('',#4861,#3902,#3903);
#3507=AXIS2_PLACEMENT_3D('',#4871,#3909,#3910);
#3508=AXIS2_PLACEMENT_3D('',#4873,#3912,#3913);
#3509=AXIS2_PLACEMENT_3D('',#4877,#3915,#3916);
#3510=AXIS2_PLACEMENT_3D('',#4879,#3918,#3919);
#3511=AXIS2_PLACEMENT_3D('',#4881,#3920,#3921);
#3512=AXIS2_PLACEMENT_3D('',#4884,#3923,#3924);
#3513=AXIS2_PLACEMENT_3D('',#4886,#3925,#3926);
#3514=AXIS2_PLACEMENT_3D('',#4887,#3927,#3928);
#3515=AXIS2_PLACEMENT_3D('',#4888,#3929,#3930);
#3516=AXIS2_PLACEMENT_3D('',#4890,#3932,#3933);
#3517=AXIS2_PLACEMENT_3D('',#4892,#3935,#3936);
#3518=AXIS2_PLACEMENT_3D('',#4894,#3938,#3939);
#3865=DIRECTION('axis',(0.,0.,1.));
#3866=DIRECTION('refdir',(1.,0.,0.));
#3867=DIRECTION('center_axis',(0.,0.,1.));
#3868=DIRECTION('ref_axis',(1.,0.,0.));
#3869=DIRECTION('',(1.,0.,0.));
#3870=DIRECTION('',(0.,-1.,0.));
#3871=DIRECTION('',(-1.,0.,0.));
#3872=DIRECTION('',(0.,1.,0.));
#3873=DIRECTION('center_axis',(0.,1.,0.));
#3874=DIRECTION('ref_axis',(-1.,0.,0.));
#3875=DIRECTION('',(0.,0.,1.));
#3876=DIRECTION('',(-1.,0.,0.));
#3877=DIRECTION('',(0.,0.,1.));
#3878=DIRECTION('center_axis',(0.,0.,1.));
#3879=DIRECTION('ref_axis',(1.,0.,0.));
#3880=DIRECTION('',(0.,-1.,0.));
#3881=DIRECTION('',(1.,0.,0.));
#3882=DIRECTION('',(0.,1.,0.));
#3883=DIRECTION('center_axis',(0.,0.,-1.));
#3884=DIRECTION('ref_axis',(1.,0.,0.));
#3885=DIRECTION('center_axis',(-1.,0.,0.));
#3886=DIRECTION('ref_axis',(0.,-1.,0.));
#3887=DIRECTION('',(0.,0.,1.));
#3888=DIRECTION('',(0.,0.707106781186548,0.707106781186548));
#3889=DIRECTION('',(0.,-1.,0.));
#3890=DIRECTION('',(0.,0.707106781186548,-0.707106781186548));
#3891=DIRECTION('',(0.,0.,1.));
#3892=DIRECTION('',(0.,-1.,0.));
#3893=DIRECTION('',(0.,0.,1.));
#3894=DIRECTION('center_axis',(0.,-1.,0.));
#3895=DIRECTION('ref_axis',(1.,0.,0.));
#3896=DIRECTION('',(1.,0.,0.));
#3897=DIRECTION('',(0.,0.,1.));
#3898=DIRECTION('center_axis',(0.,0.,1.));
#3899=DIRECTION('ref_axis',(1.,0.,0.));
#3900=DIRECTION('',(-1.,0.,0.));
#3901=DIRECTION('',(0.,1.,0.));
#3902=DIRECTION('center_axis',(1.,0.,0.));
#3903=DIRECTION('ref_axis',(0.,1.,0.));
#3904=DIRECTION('',(0.,0.,1.));
#3905=DIRECTION('',(0.,-0.707106781186548,0.707106781186548));
#3906=DIRECTION('',(0.,1.,0.));
#3907=DIRECTION('',(0.,-0.707106781186548,-0.707106781186548));
#3908=DIRECTION('',(0.,0.,1.));
#3909=DIRECTION('center_axis',(0.,-1.,0.));
#3910=DIRECTION('ref_axis',(1.,0.,0.));
#3911=DIRECTION('',(-1.,0.,0.));
#3912=DIRECTION('center_axis',(0.,-0.707106781186548,-0.707106781186548));
#3913=DIRECTION('ref_axis',(-1.,0.,0.));
#3914=DIRECTION('',(1.,0.,0.));
#3915=DIRECTION('center_axis',(0.,0.707106781186548,0.707106781186548));
#3916=DIRECTION('ref_axis',(0.,0.707106781186547,-0.707106781186547));
#3917=DIRECTION('',(1.,0.,0.));
#3918=DIRECTION('center_axis',(0.,0.,1.));
#3919=DIRECTION('ref_axis',(1.,0.,0.));
#3920=DIRECTION('center_axis',(0.,0.,-1.));
#3921=DIRECTION('ref_axis',(1.,0.,0.));
#3922=DIRECTION('',(0.,0.,1.));
#3923=DIRECTION('center_axis',(0.,0.,-1.));
#3924=DIRECTION('ref_axis',(1.,0.,0.));
#3925=DIRECTION('center_axis',(0.,-0.707106781186548,0.707106781186548));
#3926=DIRECTION('ref_axis',(0.,0.707106781186547,0.707106781186547));
#3927=DIRECTION('center_axis',(0.,0.,-1.));
#3928=DIRECTION('ref_axis',(1.,0.,0.));
#3929=DIRECTION('center_axis',(0.,0.,1.));
#3930=DIRECTION('ref_axis',(1.,0.,0.));
#3931=DIRECTION('',(-1.,0.,0.));
#3932=DIRECTION('center_axis',(0.,0.,1.));
#3933=DIRECTION('ref_axis',(1.,0.,0.));
#3934=DIRECTION('',(-1.,0.,0.));
#3935=DIRECTION('center_axis',(0.,0.707106781186548,-0.707106781186548));
#3936=DIRECTION('ref_axis',(-1.,0.,0.));
#3937=DIRECTION('',(1.,0.,0.));
#3938=DIRECTION('center_axis',(0.,1.,0.));
#3939=DIRECTION('ref_axis',(-1.,0.,0.));
#4815=CARTESIAN_POINT('',(0.,0.,0.));
#4816=CARTESIAN_POINT('Origin',(0.,0.395,0.25));
#4817=CARTESIAN_POINT('',(-0.5,0.3,0.25));
#4818=CARTESIAN_POINT('',(0.5,0.3,0.25));
#4819=CARTESIAN_POINT('',(0.25,0.3,0.25));
#4820=CARTESIAN_POINT('',(-0.5,0.5,0.25));
#4821=CARTESIAN_POINT('',(-0.5,0.5,0.25));
#4822=CARTESIAN_POINT('',(0.5,0.5,0.25));
#4823=CARTESIAN_POINT('',(0.5,0.5,0.25));
#4824=CARTESIAN_POINT('',(0.5,0.29,0.25));
#4825=CARTESIAN_POINT('Origin',(0.5,0.5,0.25));
#4826=CARTESIAN_POINT('',(-0.5,0.5,0.4));
#4827=CARTESIAN_POINT('',(-0.5,0.5,0.25));
#4828=CARTESIAN_POINT('',(0.5,0.5,0.4));
#4829=CARTESIAN_POINT('',(0.5,0.5,0.4));
#4830=CARTESIAN_POINT('',(0.5,0.5,0.25));
#4831=CARTESIAN_POINT('Origin',(0.,0.,0.4));
#4832=CARTESIAN_POINT('',(-0.5,-0.5,0.4));
#4833=CARTESIAN_POINT('',(-0.5,0.5,0.4));
#4834=CARTESIAN_POINT('',(0.5,-0.5,0.4));
#4835=CARTESIAN_POINT('',(-0.5,-0.5,0.4));
#4836=CARTESIAN_POINT('',(0.5,-0.3,0.4));
#4837=CARTESIAN_POINT('',(-0.2117,2.59257727379495E-17,0.4));
#4838=CARTESIAN_POINT('Origin',(0.,0.,0.4));
#4839=CARTESIAN_POINT('Origin',(-0.5,0.3,0.));
#4840=CARTESIAN_POINT('',(-0.5,0.3,0.15));
#4841=CARTESIAN_POINT('',(-0.5,0.3,0.));
#4842=CARTESIAN_POINT('',(-0.5,0.15,0.));
#4843=CARTESIAN_POINT('',(-0.5,0.225,0.075));
#4844=CARTESIAN_POINT('',(-0.5,-0.15,0.));
#4845=CARTESIAN_POINT('',(-0.5,0.3,0.));
#4846=CARTESIAN_POINT('',(-0.5,-0.3,0.15));
#4847=CARTESIAN_POINT('',(-0.5,-0.075,-0.075));
#4848=CARTESIAN_POINT('',(-0.5,-0.3,0.25));
#4849=CARTESIAN_POINT('',(-0.5,-0.3,0.));
#4850=CARTESIAN_POINT('',(-0.5,-0.5,0.25));
#4851=CARTESIAN_POINT('',(-0.5,-0.29,0.25));
#4852=CARTESIAN_POINT('',(-0.5,-0.5,0.25));
#4853=CARTESIAN_POINT('Origin',(-0.5,-0.5,0.25));
#4854=CARTESIAN_POINT('',(0.5,-0.5,0.25));
#4855=CARTESIAN_POINT('',(-0.5,-0.5,0.25));
#4856=CARTESIAN_POINT('',(0.5,-0.5,0.25));
#4857=CARTESIAN_POINT('Origin',(0.,-0.395,0.25));
#4858=CARTESIAN_POINT('',(0.5,-0.3,0.25));
#4859=CARTESIAN_POINT('',(-0.25,-0.3,0.25));
#4860=CARTESIAN_POINT('',(0.5,-0.5,0.25));
#4861=CARTESIAN_POINT('Origin',(0.5,-0.3,0.));
#4862=CARTESIAN_POINT('',(0.5,-0.3,0.15));
#4863=CARTESIAN_POINT('',(0.5,-0.3,0.));
#4864=CARTESIAN_POINT('',(0.5,-0.15,0.));
#4865=CARTESIAN_POINT('',(0.5,-0.225,0.075));
#4866=CARTESIAN_POINT('',(0.5,0.15,0.));
#4867=CARTESIAN_POINT('',(0.5,-0.3,0.));
#4868=CARTESIAN_POINT('',(0.5,0.3,0.15));
#4869=CARTESIAN_POINT('',(0.5,0.075,-0.075));
#4870=CARTESIAN_POINT('',(0.5,0.3,0.));
#4871=CARTESIAN_POINT('Origin',(-0.5,-0.3,0.));
#4872=CARTESIAN_POINT('',(-0.25,-0.3,0.15));
#4873=CARTESIAN_POINT('Origin',(-0.25,-0.225,0.075));
#4874=CARTESIAN_POINT('',(-0.149388386429468,-0.15,0.));
#4875=CARTESIAN_POINT('',(-0.25,-0.15,0.));
#4876=CARTESIAN_POINT('',(0.149388386429468,-0.15,0.));
#4877=CARTESIAN_POINT('Origin',(0.,0.,-0.15));
#4878=CARTESIAN_POINT('',(-0.25,-0.15,0.));
#4879=CARTESIAN_POINT('Origin',(0.,0.,-0.1));
#4880=CARTESIAN_POINT('',(-0.2117,-2.59257727379495E-17,0.));
#4881=CARTESIAN_POINT('Origin',(0.,0.,0.));
#4882=CARTESIAN_POINT('',(-0.2117,-2.59257727379495E-17,-0.1));
#4883=CARTESIAN_POINT('',(-0.149388386429468,0.15,0.));
#4884=CARTESIAN_POINT('Origin',(0.,0.,0.));
#4885=CARTESIAN_POINT('',(0.149388386429468,0.15,0.));
#4886=CARTESIAN_POINT('Origin',(0.,0.,-0.15));
#4887=CARTESIAN_POINT('Origin',(0.,0.,0.));
#4888=CARTESIAN_POINT('Origin',(0.,0.,0.));
#4889=CARTESIAN_POINT('',(0.25,0.15,0.));
#4890=CARTESIAN_POINT('Origin',(0.,0.,0.));
#4891=CARTESIAN_POINT('',(0.25,0.15,0.));
#4892=CARTESIAN_POINT('Origin',(0.25,0.225,0.075));
#4893=CARTESIAN_POINT('',(0.25,0.3,0.15));
#4894=CARTESIAN_POINT('Origin',(0.5,0.3,0.));
#5733=UNCERTAINTY_MEASURE_WITH_UNIT(LENGTH_MEASURE(0.001),#5762,
'DISTANCE_ACCURACY_VALUE',
'Maximum model space distance between geometric entities at asserted c
onnectivities');
#5745=UNCERTAINTY_MEASURE_WITH_UNIT(LENGTH_MEASURE(0.001),#5762,
'DISTANCE_ACCURACY_VALUE',
'Maximum model space distance between geometric entities at asserted c
onnectivities');
#5749=(
GEOMETRIC_REPRESENTATION_CONTEXT(3)
GLOBAL_UNCERTAINTY_ASSIGNED_CONTEXT((#5733))
GLOBAL_UNIT_ASSIGNED_CONTEXT((#5762,#5764,#5765))
REPRESENTATION_CONTEXT('','3D')
);
#5761=(
GEOMETRIC_REPRESENTATION_CONTEXT(3)
GLOBAL_UNCERTAINTY_ASSIGNED_CONTEXT((#5745))
GLOBAL_UNIT_ASSIGNED_CONTEXT((#5762,#5764,#5765))
REPRESENTATION_CONTEXT('','3D')
);
#5762=(
LENGTH_UNIT()
NAMED_UNIT(*)
SI_UNIT(.CENTI.,.METRE.)
);
#5764=(
NAMED_UNIT(*)
PLANE_ANGLE_UNIT()
SI_UNIT($,.RADIAN.)
);
#5765=(
NAMED_UNIT(*)
SI_UNIT($,.STERADIAN.)
SOLID_ANGLE_UNIT()
);
#5769=SHAPE_DEFINITION_REPRESENTATION(#5784,#5818);
#5784=PRODUCT_DEFINITION_SHAPE('',$,#5834);
#5818=SHAPE_REPRESENTATION('',(#3498),#5749);
#5830=PRODUCT_DEFINITION_CONTEXT('part definition',#5877,'design');
#5834=PRODUCT_DEFINITION('Captive slot nut','Captive slot nut',#5849,#5830);
#5849=PRODUCT_DEFINITION_FORMATION('',$,#5882);
#5877=APPLICATION_CONTEXT(
'Core Data for Automotive Mechanical Design Process');
#5878=PRODUCT_CONTEXT('part definition',#5877,'mechanical');
#5882=PRODUCT('Captive slot nut','Captive slot nut','Captive slot nut',
(#5878));
#5950=COLOUR_RGB('Black',0.12,0.14,0.17);
#5951=FILL_AREA_STYLE_COLOUR('',#5950);
#5952=FILL_AREA_STYLE('',(#5951));
#5953=SURFACE_STYLE_FILL_AREA(#5952);
#5954=SURFACE_SIDE_STYLE('',(#5953));
#5955=SURFACE_STYLE_USAGE(.BOTH.,#5954);
#5956=PRESENTATION_STYLE_ASSIGNMENT((#5955));
ENDSEC;
END-ISO-10303-21;
